ISO-10303-21;
HEADER;
/* Generated by software containing ST-Developer
 * from STEP Tools, Inc. (www.steptools.com) 
 */

FILE_DESCRIPTION(
/* description */ ('Four-bar tabletop demonstrator'),
/* implementation_level */ '2;1');

FILE_NAME(
/* name */ 'M5x14 Cap Screw.step',
/* time_stamp */ '2026-10-29T17:05:23-07:00',
/* author */ (''),
/* organization */ (''),
/* preprocessor_version */ 'ST-DEVELOPER v20.2',
/* originating_system */ 'Autodesk Translation Framework v15.17.0.0',
/* authorisation */ '');

FILE_SCHEMA (('AUTOMOTIVE_DESIGN { 1 0 10303 214 3 1 1 }'));
ENDSEC;

DATA;
#10=MECHANICAL_DESIGN_GEOMETRIC_PRESENTATION_REPRESENTATION('',(#339),#6705);
#265=CONICAL_SURFACE('',#3688,0.4,0.785398163397448);
#266=CONICAL_SURFACE('',#3692,0.41,0.785398163397448);
#267=CONICAL_SURFACE('',#3696,0.26,0.463647609000806);
#276=ORIENTED_CLOSED_SHELL('',*,#3383,.F.);
#278=BREP_WITH_VOIDS('Body1',#3384,(#276));
#309=SHAPE_REPRESENTATION_RELATIONSHIP('SRR','None',#6815,#324);
#324=ADVANCED_BREP_SHAPE_REPRESENTATION('',(#278),#6688);
#339=STYLED_ITEM('',(#6996),#278);
#415=FACE_BOUND('',#856,.T.);
#480=PLANE('',#3676);
#481=PLANE('',#3677);
#482=PLANE('',#3678);
#483=PLANE('',#3679);
#484=PLANE('',#3680);
#485=PLANE('',#3681);
#486=PLANE('',#3682);
#487=PLANE('',#3683);
#488=PLANE('',#3684);
#489=PLANE('',#3686);
#490=PLANE('',#3694);
#605=FACE_OUTER_BOUND('',#842,.T.);
#606=FACE_OUTER_BOUND('',#843,.T.);
#607=FACE_OUTER_BOUND('',#844,.T.);
#608=FACE_OUTER_BOUND('',#845,.T.);
#609=FACE_OUTER_BOUND('',#846,.T.);
#610=FACE_OUTER_BOUND('',#847,.T.);
#611=FACE_OUTER_BOUND('',#848,.T.);
#612=FACE_OUTER_BOUND('',#849,.T.);
#613=FACE_OUTER_BOUND('',#850,.T.);
#614=FACE_OUTER_BOUND('',#851,.T.);
#615=FACE_OUTER_BOUND('',#852,.T.);
#616=FACE_OUTER_BOUND('',#853,.T.);
#617=FACE_OUTER_BOUND('',#854,.T.);
#618=FACE_OUTER_BOUND('',#855,.T.);
#619=FACE_OUTER_BOUND('',#857,.T.);
#620=FACE_OUTER_BOUND('',#858,.T.);
#842=EDGE_LOOP('',(#2490,#2491,#2492,#2493));
#843=EDGE_LOOP('',(#2494,#2495,#2496,#2497));
#844=EDGE_LOOP('',(#2498,#2499,#2500,#2501));
#845=EDGE_LOOP('',(#2502,#2503,#2504,#2505));
#846=EDGE_LOOP('',(#2506,#2507,#2508,#2509));
#847=EDGE_LOOP('',(#2510,#2511,#2512,#2513));
#848=EDGE_LOOP('',(#2514,#2515,#2516,#2517,#2518,#2519));
#849=EDGE_LOOP('',(#2520,#2521,#2522,#2523,#2524,#2525));
#850=EDGE_LOOP('',(#2526));
#851=EDGE_LOOP('',(#2527));
#852=EDGE_LOOP('',(#2528,#2529,#2530,#2531));
#853=EDGE_LOOP('',(#2532,#2533,#2534,#2535));
#854=EDGE_LOOP('',(#2536,#2537,#2538,#2539));
#855=EDGE_LOOP('',(#2540));
#856=EDGE_LOOP('',(#2541));
#857=EDGE_LOOP('',(#2542,#2543,#2544,#2545));
#858=EDGE_LOOP('',(#2546,#2547,#2548,#2549));
#1090=LINE('',#5512,#1260);
#1091=LINE('',#5514,#1261);
#1092=LINE('',#5516,#1262);
#1093=LINE('',#5517,#1263);
#1094=LINE('',#5520,#1264);
#1095=LINE('',#5522,#1265);
#1096=LINE('',#5523,#1266);
#1097=LINE('',#5526,#1267);
#1098=LINE('',#5528,#1268);
#1099=LINE('',#5529,#1269);
#1100=LINE('',#5532,#1270);
#1101=LINE('',#5534,#1271);
#1102=LINE('',#5535,#1272);
#1103=LINE('',#5538,#1273);
#1104=LINE('',#5540,#1274);
#1105=LINE('',#5541,#1275);
#1106=LINE('',#5543,#1276);
#1107=LINE('',#5544,#1277);
#1108=LINE('',#5556,#1278);
#1109=LINE('',#5560,#1279);
#1110=LINE('',#5564,#1280);
#1111=LINE('',#5571,#1281);
#1112=LINE('',#5573,#1282);
#1260=VECTOR('',#4317,1.);
#1261=VECTOR('',#4318,1.);
#1262=VECTOR('',#4319,1.);
#1263=VECTOR('',#4320,1.);
#1264=VECTOR('',#4323,1.);
#1265=VECTOR('',#4324,1.);
#1266=VECTOR('',#4325,1.);
#1267=VECTOR('',#4328,1.);
#1268=VECTOR('',#4329,1.);
#1269=VECTOR('',#4330,1.);
#1270=VECTOR('',#4333,1.);
#1271=VECTOR('',#4334,1.);
#1272=VECTOR('',#4335,1.);
#1273=VECTOR('',#4338,1.);
#1274=VECTOR('',#4339,1.);
#1275=VECTOR('',#4340,1.);
#1276=VECTOR('',#4343,1.);
#1277=VECTOR('',#4344,1.);
#1278=VECTOR('',#4361,0.4);
#1279=VECTOR('',#4366,0.425);
#1280=VECTOR('',#4371,0.41);
#1281=VECTOR('',#4380,0.26);
#1282=VECTOR('',#4383,0.25);
#1445=CIRCLE('',#3685,0.24505);
#1446=CIRCLE('',#3687,0.375);
#1447=CIRCLE('',#3689,0.425);
#1448=CIRCLE('',#3691,0.425);
#1449=CIRCLE('',#3693,0.395);
#1450=CIRCLE('',#3695,0.27);
#1451=CIRCLE('',#3697,0.24505);
#1668=VERTEX_POINT('',#5510);
#1669=VERTEX_POINT('',#5511);
#1670=VERTEX_POINT('',#5513);
#1671=VERTEX_POINT('',#5515);
#1672=VERTEX_POINT('',#5519);
#1673=VERTEX_POINT('',#5521);
#1674=VERTEX_POINT('',#5525);
#1675=VERTEX_POINT('',#5527);
#1676=VERTEX_POINT('',#5531);
#1677=VERTEX_POINT('',#5533);
#1678=VERTEX_POINT('',#5537);
#1679=VERTEX_POINT('',#5539);
#1680=VERTEX_POINT('',#5548);
#1681=VERTEX_POINT('',#5551);
#1682=VERTEX_POINT('',#5554);
#1683=VERTEX_POINT('',#5558);
#1684=VERTEX_POINT('',#5562);
#1685=VERTEX_POINT('',#5566);
#1686=VERTEX_POINT('',#5569);
#1981=EDGE_CURVE('',#1668,#1669,#1090,.T.);
#1982=EDGE_CURVE('',#1669,#1670,#1091,.T.);
#1983=EDGE_CURVE('',#1670,#1671,#1092,.T.);
#1984=EDGE_CURVE('',#1668,#1671,#1093,.T.);
#1985=EDGE_CURVE('',#1669,#1672,#1094,.T.);
#1986=EDGE_CURVE('',#1672,#1673,#1095,.T.);
#1987=EDGE_CURVE('',#1673,#1670,#1096,.T.);
#1988=EDGE_CURVE('',#1672,#1674,#1097,.T.);
#1989=EDGE_CURVE('',#1674,#1675,#1098,.T.);
#1990=EDGE_CURVE('',#1675,#1673,#1099,.T.);
#1991=EDGE_CURVE('',#1674,#1676,#1100,.T.);
#1992=EDGE_CURVE('',#1676,#1677,#1101,.T.);
#1993=EDGE_CURVE('',#1677,#1675,#1102,.T.);
#1994=EDGE_CURVE('',#1676,#1678,#1103,.T.);
#1995=EDGE_CURVE('',#1678,#1679,#1104,.T.);
#1996=EDGE_CURVE('',#1679,#1677,#1105,.T.);
#1997=EDGE_CURVE('',#1678,#1668,#1106,.T.);
#1998=EDGE_CURVE('',#1671,#1679,#1107,.T.);
#1999=EDGE_CURVE('',#1680,#1680,#1445,.T.);
#2000=EDGE_CURVE('',#1681,#1681,#1446,.T.);
#2001=EDGE_CURVE('',#1682,#1682,#1447,.T.);
#2002=EDGE_CURVE('',#1682,#1681,#1108,.T.);
#2003=EDGE_CURVE('',#1683,#1683,#1448,.T.);
#2004=EDGE_CURVE('',#1683,#1682,#1109,.T.);
#2005=EDGE_CURVE('',#1684,#1684,#1449,.T.);
#2006=EDGE_CURVE('',#1684,#1683,#1110,.T.);
#2007=EDGE_CURVE('',#1685,#1685,#1450,.T.);
#2008=EDGE_CURVE('',#1686,#1686,#1451,.F.);
#2009=EDGE_CURVE('',#1686,#1685,#1111,.T.);
#2010=EDGE_CURVE('',#1680,#1686,#1112,.T.);
#2490=ORIENTED_EDGE('',*,*,#1981,.T.);
#2491=ORIENTED_EDGE('',*,*,#1982,.T.);
#2492=ORIENTED_EDGE('',*,*,#1983,.T.);
#2493=ORIENTED_EDGE('',*,*,#1984,.F.);
#2494=ORIENTED_EDGE('',*,*,#1985,.T.);
#2495=ORIENTED_EDGE('',*,*,#1986,.T.);
#2496=ORIENTED_EDGE('',*,*,#1987,.T.);
#2497=ORIENTED_EDGE('',*,*,#1982,.F.);
#2498=ORIENTED_EDGE('',*,*,#1988,.T.);
#2499=ORIENTED_EDGE('',*,*,#1989,.T.);
#2500=ORIENTED_EDGE('',*,*,#1990,.T.);
#2501=ORIENTED_EDGE('',*,*,#1986,.F.);
#2502=ORIENTED_EDGE('',*,*,#1991,.T.);
#2503=ORIENTED_EDGE('',*,*,#1992,.T.);
#2504=ORIENTED_EDGE('',*,*,#1993,.T.);
#2505=ORIENTED_EDGE('',*,*,#1989,.F.);
#2506=ORIENTED_EDGE('',*,*,#1994,.T.);
#2507=ORIENTED_EDGE('',*,*,#1995,.T.);
#2508=ORIENTED_EDGE('',*,*,#1996,.T.);
#2509=ORIENTED_EDGE('',*,*,#1992,.F.);
#2510=ORIENTED_EDGE('',*,*,#1997,.T.);
#2511=ORIENTED_EDGE('',*,*,#1984,.T.);
#2512=ORIENTED_EDGE('',*,*,#1998,.T.);
#2513=ORIENTED_EDGE('',*,*,#1995,.F.);
#2514=ORIENTED_EDGE('',*,*,#1997,.F.);
#2515=ORIENTED_EDGE('',*,*,#1994,.F.);
#2516=ORIENTED_EDGE('',*,*,#1991,.F.);
#2517=ORIENTED_EDGE('',*,*,#1988,.F.);
#2518=ORIENTED_EDGE('',*,*,#1985,.F.);
#2519=ORIENTED_EDGE('',*,*,#1981,.F.);
#2520=ORIENTED_EDGE('',*,*,#1998,.F.);
#2521=ORIENTED_EDGE('',*,*,#1983,.F.);
#2522=ORIENTED_EDGE('',*,*,#1987,.F.);
#2523=ORIENTED_EDGE('',*,*,#1990,.F.);
#2524=ORIENTED_EDGE('',*,*,#1993,.F.);
#2525=ORIENTED_EDGE('',*,*,#1996,.F.);
#2526=ORIENTED_EDGE('',*,*,#1999,.F.);
#2527=ORIENTED_EDGE('',*,*,#2000,.F.);
#2528=ORIENTED_EDGE('',*,*,#2001,.F.);
#2529=ORIENTED_EDGE('',*,*,#2002,.T.);
#2530=ORIENTED_EDGE('',*,*,#2000,.T.);
#2531=ORIENTED_EDGE('',*,*,#2002,.F.);
#2532=ORIENTED_EDGE('',*,*,#2003,.F.);
#2533=ORIENTED_EDGE('',*,*,#2004,.T.);
#2534=ORIENTED_EDGE('',*,*,#2001,.T.);
#2535=ORIENTED_EDGE('',*,*,#2004,.F.);
#2536=ORIENTED_EDGE('',*,*,#2005,.F.);
#2537=ORIENTED_EDGE('',*,*,#2006,.T.);
#2538=ORIENTED_EDGE('',*,*,#2003,.T.);
#2539=ORIENTED_EDGE('',*,*,#2006,.F.);
#2540=ORIENTED_EDGE('',*,*,#2005,.T.);
#2541=ORIENTED_EDGE('',*,*,#2007,.F.);
#2542=ORIENTED_EDGE('',*,*,#2008,.F.);
#2543=ORIENTED_EDGE('',*,*,#2009,.T.);
#2544=ORIENTED_EDGE('',*,*,#2007,.T.);
#2545=ORIENTED_EDGE('',*,*,#2009,.F.);
#2546=ORIENTED_EDGE('',*,*,#1999,.T.);
#2547=ORIENTED_EDGE('',*,*,#2010,.T.);
#2548=ORIENTED_EDGE('',*,*,#2008,.T.);
#2549=ORIENTED_EDGE('',*,*,#2010,.F.);
#3129=CYLINDRICAL_SURFACE('',#3690,0.425);
#3130=CYLINDRICAL_SURFACE('',#3698,0.24505);
#3221=ADVANCED_FACE('',(#605),#480,.F.);
#3222=ADVANCED_FACE('',(#606),#481,.F.);
#3223=ADVANCED_FACE('',(#607),#482,.F.);
#3224=ADVANCED_FACE('',(#608),#483,.F.);
#3225=ADVANCED_FACE('',(#609),#484,.F.);
#3226=ADVANCED_FACE('',(#610),#485,.F.);
#3227=ADVANCED_FACE('',(#611),#486,.F.);
#3228=ADVANCED_FACE('',(#612),#487,.F.);
#3229=ADVANCED_FACE('',(#613),#488,.F.);
#3230=ADVANCED_FACE('',(#614),#489,.T.);
#3231=ADVANCED_FACE('',(#615),#265,.T.);
#3232=ADVANCED_FACE('',(#616),#3129,.T.);
#3233=ADVANCED_FACE('',(#617),#266,.T.);
#3234=ADVANCED_FACE('',(#618,#415),#490,.T.);
#3235=ADVANCED_FACE('',(#619),#267,.T.);
#3236=ADVANCED_FACE('',(#620),#3130,.T.);
#3383=CLOSED_SHELL('',(#3221,#3222,#3223,#3224,#3225,#3226,#3227,#3228));
#3384=CLOSED_SHELL('',(#3229,#3230,#3231,#3232,#3233,#3234,#3235,#3236));
#3675=AXIS2_PLACEMENT_3D('',#5508,#4313,#4314);
#3676=AXIS2_PLACEMENT_3D('',#5509,#4315,#4316);
#3677=AXIS2_PLACEMENT_3D('',#5518,#4321,#4322);
#3678=AXIS2_PLACEMENT_3D('',#5524,#4326,#4327);
#3679=AXIS2_PLACEMENT_3D('',#5530,#4331,#4332);
#3680=AXIS2_PLACEMENT_3D('',#5536,#4336,#4337);
#3681=AXIS2_PLACEMENT_3D('',#5542,#4341,#4342);
#3682=AXIS2_PLACEMENT_3D('',#5545,#4345,#4346);
#3683=AXIS2_PLACEMENT_3D('',#5546,#4347,#4348);
#3684=AXIS2_PLACEMENT_3D('',#5547,#4349,#4350);
#3685=AXIS2_PLACEMENT_3D('',#5549,#4351,#4352);
#3686=AXIS2_PLACEMENT_3D('',#5550,#4353,#4354);
#3687=AXIS2_PLACEMENT_3D('',#5552,#4355,#4356);
#3688=AXIS2_PLACEMENT_3D('',#5553,#4357,#4358);
#3689=AXIS2_PLACEMENT_3D('',#5555,#4359,#4360);
#3690=AXIS2_PLACEMENT_3D('',#5557,#4362,#4363);
#3691=AXIS2_PLACEMENT_3D('',#5559,#4364,#4365);
#3692=AXIS2_PLACEMENT_3D('',#5561,#4367,#4368);
#3693=AXIS2_PLACEMENT_3D('',#5563,#4369,#4370);
#3694=AXIS2_PLACEMENT_3D('',#5565,#4372,#4373);
#3695=AXIS2_PLACEMENT_3D('',#5567,#4374,#4375);
#3696=AXIS2_PLACEMENT_3D('',#5568,#4376,#4377);
#3697=AXIS2_PLACEMENT_3D('',#5570,#4378,#4379);
#3698=AXIS2_PLACEMENT_3D('',#5572,#4381,#4382);
#4313=DIRECTION('axis',(0.,0.,1.));
#4314=DIRECTION('refdir',(1.,0.,0.));
#4315=DIRECTION('center_axis',(0.866025403784439,0.,-0.5));
#4316=DIRECTION('ref_axis',(0.5,0.,0.866025403784439));
#4317=DIRECTION('',(-0.5,0.,-0.866025403784439));
#4318=DIRECTION('',(0.,-1.,0.));
#4319=DIRECTION('',(0.5,0.,0.866025403784439));
#4320=DIRECTION('',(0.,-1.,0.));
#4321=DIRECTION('center_axis',(1.20185167898973E-16,0.,-1.));
#4322=DIRECTION('ref_axis',(1.,0.,1.20185167898973E-16));
#4323=DIRECTION('',(-1.,0.,-1.20185167898973E-16));
#4324=DIRECTION('',(0.,-1.,0.));
#4325=DIRECTION('',(1.,0.,1.20185167898973E-16));
#4326=DIRECTION('center_axis',(-0.866025403784439,0.,-0.5));
#4327=DIRECTION('ref_axis',(0.5,0.,-0.866025403784439));
#4328=DIRECTION('',(-0.5,0.,0.866025403784439));
#4329=DIRECTION('',(0.,-1.,0.));
#4330=DIRECTION('',(0.5,0.,-0.866025403784439));
#4331=DIRECTION('center_axis',(-0.866025403784439,0.,0.5));
#4332=DIRECTION('ref_axis',(-0.5,0.,-0.866025403784439));
#4333=DIRECTION('',(0.5,0.,0.866025403784439));
#4334=DIRECTION('',(0.,-1.,0.));
#4335=DIRECTION('',(-0.5,0.,-0.866025403784439));
#4336=DIRECTION('center_axis',(-2.40370335797945E-16,0.,1.));
#4337=DIRECTION('ref_axis',(-1.,0.,-2.40370335797945E-16));
#4338=DIRECTION('',(1.,0.,2.40370335797945E-16));
#4339=DIRECTION('',(0.,-1.,0.));
#4340=DIRECTION('',(-1.,0.,-2.40370335797945E-16));
#4341=DIRECTION('center_axis',(0.866025403784439,0.,0.5));
#4342=DIRECTION('ref_axis',(-0.5,0.,0.866025403784439));
#4343=DIRECTION('',(0.5,0.,-0.866025403784439));
#4344=DIRECTION('',(-0.5,0.,0.866025403784439));
#4345=DIRECTION('center_axis',(0.,1.,0.));
#4346=DIRECTION('ref_axis',(1.,0.,0.));
#4347=DIRECTION('center_axis',(0.,-1.,0.));
#4348=DIRECTION('ref_axis',(0.,0.,-1.));
#4349=DIRECTION('center_axis',(0.,1.,0.));
#4350=DIRECTION('ref_axis',(1.,0.,0.));
#4351=DIRECTION('center_axis',(0.,1.,0.));
#4352=DIRECTION('ref_axis',(1.,0.,0.));
#4353=DIRECTION('center_axis',(0.,1.,0.));
#4354=DIRECTION('ref_axis',(0.,0.,1.));
#4355=DIRECTION('center_axis',(0.,-1.,0.));
#4356=DIRECTION('ref_axis',(1.,0.,0.));
#4357=DIRECTION('center_axis',(0.,-1.,0.));
#4358=DIRECTION('ref_axis',(1.,0.,0.));
#4359=DIRECTION('center_axis',(0.,-1.,0.));
#4360=DIRECTION('ref_axis',(1.,0.,0.));
#4361=DIRECTION('',(0.707106781186548,0.707106781186547,8.65956056235493E-17));
#4362=DIRECTION('center_axis',(0.,-1.,0.));
#4363=DIRECTION('ref_axis',(1.,0.,0.));
#4364=DIRECTION('center_axis',(0.,-1.,0.));
#4365=DIRECTION('ref_axis',(1.,0.,0.));
#4366=DIRECTION('',(0.,1.,0.));
#4367=DIRECTION('center_axis',(0.,1.,0.));
#4368=DIRECTION('ref_axis',(1.,0.,0.));
#4369=DIRECTION('center_axis',(0.,-1.,0.));
#4370=DIRECTION('ref_axis',(1.,0.,0.));
#4371=DIRECTION('',(-0.707106781186547,0.707106781186548,-8.65956056235493E-17));
#4372=DIRECTION('center_axis',(0.,-1.,0.));
#4373=DIRECTION('ref_axis',(0.,0.,-1.));
#4374=DIRECTION('center_axis',(0.,-1.,0.));
#4375=DIRECTION('ref_axis',(1.,0.,0.));
#4376=DIRECTION('center_axis',(0.,1.,0.));
#4377=DIRECTION('ref_axis',(1.,0.,0.));
#4378=DIRECTION('center_axis',(0.,1.,0.));
#4379=DIRECTION('ref_axis',(1.,0.,0.));
#4380=DIRECTION('',(-0.447213595499958,0.894427190999916,-5.47678698264203E-17));
#4381=DIRECTION('center_axis',(0.,-1.,0.));
#4382=DIRECTION('ref_axis',(1.,0.,0.));
#4383=DIRECTION('',(0.,1.,0.));
#5508=CARTESIAN_POINT('',(0.,0.,0.));
#5509=CARTESIAN_POINT('Origin',(0.115470053837925,-0.5,-0.2));
#5510=CARTESIAN_POINT('',(0.23094010767585,-0.5,0.));
#5511=CARTESIAN_POINT('',(0.115470053837925,-0.5,-0.2));
#5512=CARTESIAN_POINT('',(0.23094010767585,-0.5,0.));
#5513=CARTESIAN_POINT('',(0.115470053837925,-0.8,-0.2));
#5514=CARTESIAN_POINT('',(0.115470053837925,-0.5,-0.2));
#5515=CARTESIAN_POINT('',(0.23094010767585,-0.8,0.));
#5516=CARTESIAN_POINT('',(0.23094010767585,-0.8,0.));
#5517=CARTESIAN_POINT('',(0.23094010767585,-0.5,0.));
#5518=CARTESIAN_POINT('Origin',(-0.115470053837925,-0.5,-0.2));
#5519=CARTESIAN_POINT('',(-0.115470053837925,-0.5,-0.2));
#5520=CARTESIAN_POINT('',(0.115470053837925,-0.5,-0.2));
#5521=CARTESIAN_POINT('',(-0.115470053837925,-0.8,-0.2));
#5522=CARTESIAN_POINT('',(-0.115470053837925,-0.5,-0.2));
#5523=CARTESIAN_POINT('',(0.115470053837925,-0.8,-0.2));
#5524=CARTESIAN_POINT('Origin',(-0.23094010767585,-0.5,-2.77555756156289E-17));
#5525=CARTESIAN_POINT('',(-0.23094010767585,-0.5,-2.82820063659975E-17));
#5526=CARTESIAN_POINT('',(-0.115470053837925,-0.5,-0.2));
#5527=CARTESIAN_POINT('',(-0.23094010767585,-0.8,-2.77555756156289E-17));
#5528=CARTESIAN_POINT('',(-0.23094010767585,-0.5,-2.82820063659975E-17));
#5529=CARTESIAN_POINT('',(-0.115470053837925,-0.8,-0.2));
#5530=CARTESIAN_POINT('Origin',(-0.115470053837925,-0.5,0.2));
#5531=CARTESIAN_POINT('',(-0.115470053837925,-0.5,0.2));
#5532=CARTESIAN_POINT('',(-0.23094010767585,-0.5,-2.82820063659975E-17));
#5533=CARTESIAN_POINT('',(-0.115470053837925,-0.8,0.2));
#5534=CARTESIAN_POINT('',(-0.115470053837925,-0.5,0.2));
#5535=CARTESIAN_POINT('',(-0.23094010767585,-0.8,-2.82820063659975E-17));
#5536=CARTESIAN_POINT('Origin',(0.115470053837925,-0.5,0.2));
#5537=CARTESIAN_POINT('',(0.115470053837925,-0.5,0.2));
#5538=CARTESIAN_POINT('',(-0.115470053837925,-0.5,0.2));
#5539=CARTESIAN_POINT('',(0.115470053837925,-0.8,0.2));
#5540=CARTESIAN_POINT('',(0.115470053837925,-0.5,0.2));
#5541=CARTESIAN_POINT('',(-0.115470053837925,-0.8,0.2));
#5542=CARTESIAN_POINT('Origin',(0.23094010767585,-0.5,0.));
#5543=CARTESIAN_POINT('',(0.115470053837925,-0.5,0.2));
#5544=CARTESIAN_POINT('',(0.115470053837925,-0.8,0.2));
#5545=CARTESIAN_POINT('Origin',(0.,-0.5,0.));
#5546=CARTESIAN_POINT('Origin',(0.,-0.8,0.));
#5547=CARTESIAN_POINT('Origin',(0.,-1.4,0.));
#5548=CARTESIAN_POINT('',(-0.24505,-1.4,3.00099698131059E-17));
#5549=CARTESIAN_POINT('Origin',(0.,-1.4,0.));
#5550=CARTESIAN_POINT('Origin',(0.375,0.5,0.));
#5551=CARTESIAN_POINT('',(-0.375,0.5,-4.59242549680257E-17));
#5552=CARTESIAN_POINT('Origin',(0.,0.5,0.));
#5553=CARTESIAN_POINT('Origin',(0.,0.475,0.));
#5554=CARTESIAN_POINT('',(-0.425,0.45,-5.20474889637625E-17));
#5555=CARTESIAN_POINT('Origin',(0.,0.45,0.));
#5556=CARTESIAN_POINT('',(-0.4,0.475,-4.89858719658941E-17));
#5557=CARTESIAN_POINT('Origin',(0.,0.24,0.));
#5558=CARTESIAN_POINT('',(-0.425,0.0299999999999998,-5.20474889637625E-17));
#5559=CARTESIAN_POINT('Origin',(0.,0.0299999999999998,0.));
#5560=CARTESIAN_POINT('',(-0.425,0.24,-5.20474889637625E-17));
#5561=CARTESIAN_POINT('Origin',(0.,0.0150000000000001,0.));
#5562=CARTESIAN_POINT('',(-0.395,4.85722573273506E-17,-4.83735485663204E-17));
#5563=CARTESIAN_POINT('Origin',(0.,0.,0.));
#5564=CARTESIAN_POINT('',(-0.41,0.0150000000000001,-5.02105187650415E-17));
#5565=CARTESIAN_POINT('Origin',(0.27,0.,0.));
#5566=CARTESIAN_POINT('',(-0.27,0.,-3.30654635769785E-17));
#5567=CARTESIAN_POINT('Origin',(0.,0.,0.));
#5568=CARTESIAN_POINT('Origin',(0.,-0.02,0.));
#5569=CARTESIAN_POINT('',(-0.24505,-0.0498999999999999,3.00099698131059E-17));
#5570=CARTESIAN_POINT('Origin',(0.,-0.0498999999999999,0.));
#5571=CARTESIAN_POINT('',(-0.26,-0.02,-3.18408167778312E-17));
#5572=CARTESIAN_POINT('Origin',(0.,-0.995,0.));
#5573=CARTESIAN_POINT('',(-0.24505,-0.995,-3.00099698131059E-17));
#6666=UNCERTAINTY_MEASURE_WITH_UNIT(LENGTH_MEASURE(0.001),#6706,
'DISTANCE_ACCURACY_VALUE',
'Maximum model space distance between geometric entities at asserted c
onnectivities');
#6683=UNCERTAINTY_MEASURE_WITH_UNIT(LENGTH_MEASURE(0.001),#6706,
'DISTANCE_ACCURACY_VALUE',
'Maximum model space distance between geometric entities at asserted c
onnectivities');
#6688=(
GEOMETRIC_REPRESENTATION_CONTEXT(3)
GLOBAL_UNCERTAINTY_ASSIGNED_CONTEXT((#6666))
GLOBAL_UNIT_ASSIGNED_CONTEXT((#6706,#6708,#6709))
REPRESENTATION_CONTEXT('','3D')
);
#6705=(
GEOMETRIC_REPRESENTATION_CONTEXT(3)
GLOBAL_UNCERTAINTY_ASSIGNED_CONTEXT((#6683))
GLOBAL_UNIT_ASSIGNED_CONTEXT((#6706,#6708,#6709))
REPRESENTATION_CONTEXT('','3D')
);
#6706=(
LENGTH_UNIT()
NAMED_UNIT(*)
SI_UNIT(.CENTI.,.METRE.)
);
#6708=(
NAMED_UNIT(*)
PLANE_ANGLE_UNIT()
SI_UNIT($,.RADIAN.)
);
#6709=(
NAMED_UNIT(*)
SI_UNIT($,.STERADIAN.)
SOLID_ANGLE_UNIT()
);
#6714=SHAPE_DEFINITION_REPRESENTATION(#6735,#6815);
#6735=PRODUCT_DEFINITION_SHAPE('',$,#6837);
#6815=SHAPE_REPRESENTATION('',(#3675),#6688);
#6832=PRODUCT_DEFINITION_CONTEXT('part definition',#6897,'design');
#6837=PRODUCT_DEFINITION('M5x14 Cap Screw','M5x14 Cap Screw',#6858,#6832);
#6858=PRODUCT_DEFINITION_FORMATION('',$,#6903);
#6897=APPLICATION_CONTEXT(
'Core Data for Automotive Mechanical Design Process');
#6898=PRODUCT_CONTEXT('part definition',#6897,'mechanical');
#6903=PRODUCT('M5x14 Cap Screw','M5x14 Cap Screw','M5x14 Cap Screw',(#6898));
#6990=COLOUR_RGB('Black',0.12,0.14,0.17);
#6991=FILL_AREA_STYLE_COLOUR('',#6990);
#6992=FILL_AREA_STYLE('',(#6991));
#6993=SURFACE_STYLE_FILL_AREA(#6992);
#6994=SURFACE_SIDE_STYLE('',(#6993));
#6995=SURFACE_STYLE_USAGE(.BOTH.,#6994);
#6996=PRESENTATION_STYLE_ASSIGNMENT((#6995));
ENDSEC;
END-ISO-10303-21;
